ISO-10303-21;
HEADER;
/* Generated by software containing ST-Developer
 * from STEP Tools, Inc. (www.steptools.com) 
 */
/* OPTION: using custom renumber hook */

FILE_DESCRIPTION(
/* description */ ('STEP AP242 Edition 2', 'CAx-IF Rec.Pracs.---Representation and Presentation of Product Manufa
cturing Information (PMI)---4.0---2014-10-13', 'CAx-IF Rec.Pracs.---3D Tessellated Geometry---0.4---2014-09-14', '2;1', 'CAx-IF Rec.Pracs.---User Defined Attributes---1.5---2016-08-15'),
/* implementation_level */ '2;1');

FILE_NAME(
/* name */ 'Part 1__PD8592.step',
/* time_stamp */ '2026-10-07T00:00:55Z',
/* author */ (''),
/* organization */ (''),
/* preprocessor_version */ 'ST-DEVELOPER v20',
/* originating_system */ 'ONSHAPE BY PTC INC, 1.221',
/* authorisation */ '  ');

FILE_SCHEMA (('AP242_MANAGED_MODEL_BASED_3D_ENGINEERING_MIM_LF { 1 0 10303 442 3 1 4 }'));
ENDSEC;

DATA;
#119=SHAPE_REPRESENTATION_RELATIONSHIP('','',#4475,#130);
#130=ADVANCED_BREP_SHAPE_REPRESENTATION('',(#4451),#8538);
#207=CYLINDRICAL_SURFACE('',#4523,0.039);
#208=CYLINDRICAL_SURFACE('',#4527,0.0355);
#322=CIRCLE('',#4524,0.039);
#323=CIRCLE('',#4525,0.039);
#324=CIRCLE('',#4528,0.0355);
#325=CIRCLE('',#4529,0.0355);
#775=ORIENTED_EDGE('',*,*,#1907,.T.);
#776=ORIENTED_EDGE('',*,*,#1908,.F.);
#777=ORIENTED_EDGE('',*,*,#1909,.F.);
#778=ORIENTED_EDGE('',*,*,#1910,.T.);
#779=ORIENTED_EDGE('',*,*,#1911,.T.);
#780=ORIENTED_EDGE('',*,*,#1912,.F.);
#781=ORIENTED_EDGE('',*,*,#1913,.F.);
#782=ORIENTED_EDGE('',*,*,#1908,.T.);
#783=ORIENTED_EDGE('',*,*,#1914,.T.);
#784=ORIENTED_EDGE('',*,*,#1915,.F.);
#785=ORIENTED_EDGE('',*,*,#1916,.F.);
#786=ORIENTED_EDGE('',*,*,#1912,.T.);
#787=ORIENTED_EDGE('',*,*,#1917,.T.);
#788=ORIENTED_EDGE('',*,*,#1910,.F.);
#789=ORIENTED_EDGE('',*,*,#1918,.F.);
#790=ORIENTED_EDGE('',*,*,#1915,.T.);
#791=ORIENTED_EDGE('',*,*,#1909,.T.);
#792=ORIENTED_EDGE('',*,*,#1913,.T.);
#793=ORIENTED_EDGE('',*,*,#1916,.T.);
#794=ORIENTED_EDGE('',*,*,#1918,.T.);
#795=ORIENTED_EDGE('',*,*,#1907,.F.);
#796=ORIENTED_EDGE('',*,*,#1917,.F.);
#797=ORIENTED_EDGE('',*,*,#1914,.F.);
#798=ORIENTED_EDGE('',*,*,#1911,.F.);
#1907=EDGE_CURVE('',#2480,#2481,#322,.T.);
#1908=EDGE_CURVE('',#2482,#2481,#2846,.T.);
#1909=EDGE_CURVE('',#2483,#2482,#323,.T.);
#1910=EDGE_CURVE('',#2483,#2480,#2847,.T.);
#1911=EDGE_CURVE('',#2481,#2484,#2848,.T.);
#1912=EDGE_CURVE('',#2485,#2484,#2849,.T.);
#1913=EDGE_CURVE('',#2482,#2485,#2850,.T.);
#1914=EDGE_CURVE('',#2484,#2486,#324,.T.);
#1915=EDGE_CURVE('',#2487,#2486,#2851,.T.);
#1916=EDGE_CURVE('',#2485,#2487,#325,.T.);
#1917=EDGE_CURVE('',#2486,#2480,#2852,.T.);
#1918=EDGE_CURVE('',#2487,#2483,#2853,.T.);
#2480=VERTEX_POINT('',#6529);
#2481=VERTEX_POINT('',#6530);
#2482=VERTEX_POINT('',#6532);
#2483=VERTEX_POINT('',#6534);
#2484=VERTEX_POINT('',#6538);
#2485=VERTEX_POINT('',#6540);
#2486=VERTEX_POINT('',#6544);
#2487=VERTEX_POINT('',#6546);
#2846=LINE('',#6531,#3024);
#2847=LINE('',#6535,#3025);
#2848=LINE('',#6537,#3026);
#2849=LINE('',#6539,#3027);
#2850=LINE('',#6541,#3028);
#2851=LINE('',#6545,#3029);
#2852=LINE('',#6549,#3030);
#2853=LINE('',#6550,#3031);
#3024=VECTOR('',#5158,1.);
#3025=VECTOR('',#5161,1.);
#3026=VECTOR('',#5164,1.);
#3027=VECTOR('',#5165,1.);
#3028=VECTOR('',#5166,1.);
#3029=VECTOR('',#5171,1.);
#3030=VECTOR('',#5176,1.);
#3031=VECTOR('',#5177,1.);
#3220=EDGE_LOOP('',(#775,#776,#777,#778));
#3221=EDGE_LOOP('',(#779,#780,#781,#782));
#3222=EDGE_LOOP('',(#783,#784,#785,#786));
#3223=EDGE_LOOP('',(#787,#788,#789,#790));
#3224=EDGE_LOOP('',(#791,#792,#793,#794));
#3225=EDGE_LOOP('',(#795,#796,#797,#798));
#3597=FACE_BOUND('',#3220,.T.);
#3598=FACE_BOUND('',#3221,.T.);
#3599=FACE_BOUND('',#3222,.T.);
#3600=FACE_BOUND('',#3223,.T.);
#3601=FACE_BOUND('',#3224,.T.);
#3602=FACE_BOUND('',#3225,.T.);
#3955=PLANE('',#4526);
#3956=PLANE('',#4530);
#3957=PLANE('',#4531);
#3958=PLANE('',#4532);
#4058=ADVANCED_FACE('',(#3597),#207,.T.);
#4059=ADVANCED_FACE('',(#3598),#3955,.F.);
#4060=ADVANCED_FACE('',(#3599),#208,.F.);
#4061=ADVANCED_FACE('',(#3600),#3956,.F.);
#4062=ADVANCED_FACE('',(#3601),#3957,.T.);
#4063=ADVANCED_FACE('',(#3602),#3958,.F.);
#4325=CLOSED_SHELL('',(#4058,#4059,#4060,#4061,#4062,#4063));
#4336=STYLED_ITEM('',(#4347),#4451);
#4347=PRESENTATION_STYLE_ASSIGNMENT((#4363));
#4363=SURFACE_STYLE_USAGE(.BOTH.,#4379);
#4379=SURFACE_SIDE_STYLE('',(#4395));
#4395=SURFACE_STYLE_FILL_AREA(#4411);
#4411=FILL_AREA_STYLE('',(#4427));
#4427=FILL_AREA_STYLE_COLOUR('',#4443);
#4443=COLOUR_RGB('', 0.40784314, 0.44705882, 0.49803922);
#4451=MANIFOLD_SOLID_BREP('Part 1',#4325);
#4463=SHAPE_DEFINITION_REPRESENTATION(#8567,#4475);
#4475=SHAPE_REPRESENTATION('Part 1',(#4484),#8538);
#4484=AXIS2_PLACEMENT_3D('',#6402,#5064,#5065);
#4523=AXIS2_PLACEMENT_3D('',#6527,#5154,#5155);
#4524=AXIS2_PLACEMENT_3D('',#6528,#5156,#5157);
#4525=AXIS2_PLACEMENT_3D('',#6533,#5159,#5160);
#4526=AXIS2_PLACEMENT_3D('',#6536,#5162,#5163);
#4527=AXIS2_PLACEMENT_3D('',#6542,#5167,#5168);
#4528=AXIS2_PLACEMENT_3D('',#6543,#5169,#5170);
#4529=AXIS2_PLACEMENT_3D('',#6547,#5172,#5173);
#4530=AXIS2_PLACEMENT_3D('',#6548,#5174,#5175);
#4531=AXIS2_PLACEMENT_3D('',#6551,#5178,#5179);
#4532=AXIS2_PLACEMENT_3D('',#6552,#5180,#5181);
#5064=DIRECTION('',(0.,0.,1.));
#5065=DIRECTION('',(1.,0.,0.));
#5154=DIRECTION('',(0.,-1.,0.));
#5155=DIRECTION('',(0.,0.,-1.));
#5156=DIRECTION('',(0.,1.,0.));
#5157=DIRECTION('',(0.,0.,1.));
#5158=DIRECTION('',(0.,-1.,0.));
#5159=DIRECTION('',(0.,1.,0.));
#5160=DIRECTION('',(0.,0.,1.));
#5161=DIRECTION('',(0.,-1.,0.));
#5162=DIRECTION('',(1.,0.,2.45338361172824E-16));
#5163=DIRECTION('',(2.45338361172824E-16,0.,-1.));
#5164=DIRECTION('',(-2.45338361172824E-16,0.,1.));
#5165=DIRECTION('',(0.,-1.,0.));
#5166=DIRECTION('',(-2.45338361172824E-16,0.,1.));
#5167=DIRECTION('',(0.,-1.,0.));
#5168=DIRECTION('',(0.,0.,-1.));
#5169=DIRECTION('',(0.,-1.,0.));
#5170=DIRECTION('',(0.,0.,1.));
#5171=DIRECTION('',(0.,-1.,0.));
#5172=DIRECTION('',(0.,-1.,0.));
#5173=DIRECTION('',(0.,0.,1.));
#5174=DIRECTION('',(-1.,0.,-2.45338361172824E-16));
#5175=DIRECTION('',(-2.45338361172824E-16,0.,1.));
#5176=DIRECTION('',(2.45338361172824E-16,0.,-1.));
#5177=DIRECTION('',(2.45338361172824E-16,0.,-1.));
#5178=DIRECTION('',(0.,1.,0.));
#5179=DIRECTION('',(0.,0.,1.));
#5180=DIRECTION('',(0.,1.,0.));
#5181=DIRECTION('',(0.,0.,1.));
#6402=CARTESIAN_POINT('',(0.,0.,0.));
#6527=CARTESIAN_POINT('',(0.,0.00131,0.));
#6528=CARTESIAN_POINT('',(0.,-0.00131,0.));
#6529=CARTESIAN_POINT('',(-0.00525,-0.00131,-0.0386450190839648));
#6530=CARTESIAN_POINT('',(0.00525,-0.00131,-0.0386450190839648));
#6531=CARTESIAN_POINT('',(0.00525,0.00131,-0.0386450190839648));
#6532=CARTESIAN_POINT('',(0.00525,0.00131,-0.0386450190839648));
#6533=CARTESIAN_POINT('',(0.,0.00131,0.));
#6534=CARTESIAN_POINT('',(-0.00525,0.00131,-0.0386450190839648));
#6535=CARTESIAN_POINT('',(-0.00525,0.00131,-0.0386450190839648));
#6536=CARTESIAN_POINT('',(0.00525,0.00131,-0.0386450190839648));
#6537=CARTESIAN_POINT('',(0.00525,-0.00131,-0.0386450190839648));
#6538=CARTESIAN_POINT('',(0.00525,-0.00131,-0.0351096496707102));
#6539=CARTESIAN_POINT('',(0.00525,0.00131,-0.0351096496707102));
#6540=CARTESIAN_POINT('',(0.00525,0.00131,-0.0351096496707102));
#6541=CARTESIAN_POINT('',(0.00525,0.00131,-0.0386450190839648));
#6542=CARTESIAN_POINT('',(0.,0.00131,0.));
#6543=CARTESIAN_POINT('',(0.,-0.00131,0.));
#6544=CARTESIAN_POINT('',(-0.00525,-0.00131,-0.0351096496707102));
#6545=CARTESIAN_POINT('',(-0.00525,0.00131,-0.0351096496707102));
#6546=CARTESIAN_POINT('',(-0.00525,0.00131,-0.0351096496707102));
#6547=CARTESIAN_POINT('',(0.,0.00131,0.));
#6548=CARTESIAN_POINT('',(-0.00525,0.00131,-0.0386450190839648));
#6549=CARTESIAN_POINT('',(-0.00525,-0.00131,-0.0386450190839648));
#6550=CARTESIAN_POINT('',(-0.00525,0.00131,-0.0386450190839648));
#6551=CARTESIAN_POINT('',(0.,0.00131,0.));
#6552=CARTESIAN_POINT('',(0.,-0.00131,0.));
#8534=MECHANICAL_DESIGN_GEOMETRIC_PRESENTATION_REPRESENTATION('',(#4336),#8535);
#8535=(
GEOMETRIC_REPRESENTATION_CONTEXT(3)
GLOBAL_UNCERTAINTY_ASSIGNED_CONTEXT((#8547))
GLOBAL_UNIT_ASSIGNED_CONTEXT((#8561,#8560,#8559))
REPRESENTATION_CONTEXT('MAS-680','TOP_LEVEL_ASSEMBLY_PART')
);
#8538=(
GEOMETRIC_REPRESENTATION_CONTEXT(3)
GLOBAL_UNCERTAINTY_ASSIGNED_CONTEXT((#8550))
GLOBAL_UNIT_ASSIGNED_CONTEXT((#8561,#8560,#8559))
REPRESENTATION_CONTEXT('Part 1','COMPONENT_PART')
);
#8547=UNCERTAINTY_MEASURE_WITH_UNIT(LENGTH_MEASURE(1.E-8),#8561,
'DISTANCE_ACCURACY_VALUE','Maximum Tolerance applied to model');
#8550=UNCERTAINTY_MEASURE_WITH_UNIT(LENGTH_MEASURE(1.E-8),#8561,
'DISTANCE_ACCURACY_VALUE','Maximum Tolerance applied to model');
#8559=(
NAMED_UNIT(*)
SI_UNIT($,.STERADIAN.)
SOLID_ANGLE_UNIT()
);
#8560=(
NAMED_UNIT(*)
PLANE_ANGLE_UNIT()
SI_UNIT($,.RADIAN.)
);
#8561=(
LENGTH_UNIT()
NAMED_UNIT(*)
SI_UNIT($,.METRE.)
);
#8567=PRODUCT_DEFINITION_SHAPE('','',#8592);
#8592=PRODUCT_DEFINITION('','',#8616,#8604);
#8604=PRODUCT_DEFINITION_CONTEXT('',#8674,'design');
#8616=PRODUCT_DEFINITION_FORMATION_WITH_SPECIFIED_SOURCE('','',#8640,
 .NOT_KNOWN.);
#8640=PRODUCT('Part 1','Part 1','Part 1',(#8664));
#8664=PRODUCT_CONTEXT('',#8674,'mechanical');
#8674=APPLICATION_CONTEXT('managed model based 3d engineering');
ENDSEC;
END-ISO-10303-21;
